ISO-10303-21;
HEADER;
/* Generated by software containing ST-Developer
 * from STEP Tools, Inc. (www.steptools.com) 
 */

FILE_DESCRIPTION(
/* description */ ('Jaw-coupled motor to shaft test stand'),
/* implementation_level */ '2;1');

FILE_NAME(
/* name */ 'M3x10 motor screw (3).step',
/* time_stamp */ '2026-10-27T10:46:06-07:00',
/* author */ (''),
/* organization */ (''),
/* preprocessor_version */ 'ST-DEVELOPER v20.2',
/* originating_system */ 'Autodesk Translation Framework v15.17.0.0',
/* authorisation */ '');

FILE_SCHEMA (('AUTOMOTIVE_DESIGN { 1 0 10303 214 3 1 1 }'));
ENDSEC;

DATA;
#10=MECHANICAL_DESIGN_GEOMETRIC_PRESENTATION_REPRESENTATION('',(#352),#19361);
#288=SHAPE_REPRESENTATION_RELATIONSHIP('SRR','None',#19502,#320);
#320=ADVANCED_BREP_SHAPE_REPRESENTATION('',(#385),#19338);
#352=STYLED_ITEM('',(#19753),#385);
#385=MANIFOLD_SOLID_BREP('Body1',#10996);
#450=FACE_BOUND('',#1805,.T.);
#451=FACE_BOUND('',#1808,.T.);
#591=PLANE('',#11562);
#592=PLANE('',#11563);
#593=PLANE('',#11564);
#594=PLANE('',#11565);
#595=PLANE('',#11566);
#596=PLANE('',#11567);
#597=PLANE('',#11568);
#598=PLANE('',#11569);
#599=PLANE('',#11574);
#600=PLANE('',#11577);
#1130=FACE_OUTER_BOUND('',#1797,.T.);
#1131=FACE_OUTER_BOUND('',#1798,.T.);
#1132=FACE_OUTER_BOUND('',#1799,.T.);
#1133=FACE_OUTER_BOUND('',#1800,.T.);
#1134=FACE_OUTER_BOUND('',#1801,.T.);
#1135=FACE_OUTER_BOUND('',#1802,.T.);
#1136=FACE_OUTER_BOUND('',#1803,.T.);
#1137=FACE_OUTER_BOUND('',#1804,.T.);
#1138=FACE_OUTER_BOUND('',#1806,.T.);
#1139=FACE_OUTER_BOUND('',#1807,.T.);
#1140=FACE_OUTER_BOUND('',#1809,.T.);
#1141=FACE_OUTER_BOUND('',#1810,.T.);
#1797=EDGE_LOOP('',(#7784,#7785,#7786,#7787));
#1798=EDGE_LOOP('',(#7788,#7789,#7790,#7791));
#1799=EDGE_LOOP('',(#7792,#7793,#7794,#7795));
#1800=EDGE_LOOP('',(#7796,#7797,#7798,#7799));
#1801=EDGE_LOOP('',(#7800,#7801,#7802,#7803));
#1802=EDGE_LOOP('',(#7804,#7805,#7806,#7807));
#1803=EDGE_LOOP('',(#7808,#7809,#7810,#7811,#7812,#7813));
#1804=EDGE_LOOP('',(#7814));
#1805=EDGE_LOOP('',(#7815));
#1806=EDGE_LOOP('',(#7816,#7817,#7818,#7819));
#1807=EDGE_LOOP('',(#7820));
#1808=EDGE_LOOP('',(#7821,#7822,#7823,#7824,#7825,#7826));
#1809=EDGE_LOOP('',(#7827,#7828,#7829,#7830));
#1810=EDGE_LOOP('',(#7831));
#2528=LINE('',#15918,#3681);
#2529=LINE('',#15920,#3682);
#2530=LINE('',#15922,#3683);
#2531=LINE('',#15923,#3684);
#2532=LINE('',#15926,#3685);
#2533=LINE('',#15928,#3686);
#2534=LINE('',#15929,#3687);
#2535=LINE('',#15932,#3688);
#2536=LINE('',#15934,#3689);
#2537=LINE('',#15935,#3690);
#2538=LINE('',#15938,#3691);
#2539=LINE('',#15940,#3692);
#2540=LINE('',#15941,#3693);
#2541=LINE('',#15944,#3694);
#2542=LINE('',#15946,#3695);
#2543=LINE('',#15947,#3696);
#2544=LINE('',#15949,#3697);
#2545=LINE('',#15950,#3698);
#2546=LINE('',#15960,#3699);
#2547=LINE('',#15964,#3700);
#3681=VECTOR('',#12873,1.);
#3682=VECTOR('',#12874,1.);
#3683=VECTOR('',#12875,1.);
#3684=VECTOR('',#12876,1.);
#3685=VECTOR('',#12879,1.);
#3686=VECTOR('',#12880,1.);
#3687=VECTOR('',#12881,1.);
#3688=VECTOR('',#12884,1.);
#3689=VECTOR('',#12885,1.);
#3690=VECTOR('',#12886,1.);
#3691=VECTOR('',#12889,1.);
#3692=VECTOR('',#12890,1.);
#3693=VECTOR('',#12891,1.);
#3694=VECTOR('',#12894,1.);
#3695=VECTOR('',#12895,1.);
#3696=VECTOR('',#12896,1.);
#3697=VECTOR('',#12899,1.);
#3698=VECTOR('',#12900,1.);
#3699=VECTOR('',#12913,0.275);
#3700=VECTOR('',#12918,0.15);
#4747=CIRCLE('',#11570,0.275);
#4748=CIRCLE('',#11571,0.15);
#4749=CIRCLE('',#11573,0.275);
#4750=CIRCLE('',#11576,0.15);
#5089=VERTEX_POINT('',#15916);
#5090=VERTEX_POINT('',#15917);
#5091=VERTEX_POINT('',#15919);
#5092=VERTEX_POINT('',#15921);
#5093=VERTEX_POINT('',#15925);
#5094=VERTEX_POINT('',#15927);
#5095=VERTEX_POINT('',#15931);
#5096=VERTEX_POINT('',#15933);
#5097=VERTEX_POINT('',#15937);
#5098=VERTEX_POINT('',#15939);
#5099=VERTEX_POINT('',#15943);
#5100=VERTEX_POINT('',#15945);
#5101=VERTEX_POINT('',#15953);
#5102=VERTEX_POINT('',#15955);
#5103=VERTEX_POINT('',#15958);
#5104=VERTEX_POINT('',#15963);
#6103=EDGE_CURVE('',#5089,#5090,#2528,.T.);
#6104=EDGE_CURVE('',#5091,#5089,#2529,.T.);
#6105=EDGE_CURVE('',#5091,#5092,#2530,.T.);
#6106=EDGE_CURVE('',#5092,#5090,#2531,.T.);
#6107=EDGE_CURVE('',#5090,#5093,#2532,.T.);
#6108=EDGE_CURVE('',#5092,#5094,#2533,.T.);
#6109=EDGE_CURVE('',#5094,#5093,#2534,.T.);
#6110=EDGE_CURVE('',#5093,#5095,#2535,.T.);
#6111=EDGE_CURVE('',#5094,#5096,#2536,.T.);
#6112=EDGE_CURVE('',#5096,#5095,#2537,.T.);
#6113=EDGE_CURVE('',#5095,#5097,#2538,.T.);
#6114=EDGE_CURVE('',#5096,#5098,#2539,.T.);
#6115=EDGE_CURVE('',#5098,#5097,#2540,.T.);
#6116=EDGE_CURVE('',#5097,#5099,#2541,.T.);
#6117=EDGE_CURVE('',#5098,#5100,#2542,.T.);
#6118=EDGE_CURVE('',#5100,#5099,#2543,.T.);
#6119=EDGE_CURVE('',#5099,#5089,#2544,.T.);
#6120=EDGE_CURVE('',#5100,#5091,#2545,.T.);
#6121=EDGE_CURVE('',#5101,#5101,#4747,.T.);
#6122=EDGE_CURVE('',#5102,#5102,#4748,.T.);
#6123=EDGE_CURVE('',#5103,#5103,#4749,.T.);
#6124=EDGE_CURVE('',#5103,#5101,#2546,.T.);
#6125=EDGE_CURVE('',#5102,#5104,#2547,.T.);
#6126=EDGE_CURVE('',#5104,#5104,#4750,.T.);
#7784=ORIENTED_EDGE('',*,*,#6103,.F.);
#7785=ORIENTED_EDGE('',*,*,#6104,.F.);
#7786=ORIENTED_EDGE('',*,*,#6105,.T.);
#7787=ORIENTED_EDGE('',*,*,#6106,.T.);
#7788=ORIENTED_EDGE('',*,*,#6107,.F.);
#7789=ORIENTED_EDGE('',*,*,#6106,.F.);
#7790=ORIENTED_EDGE('',*,*,#6108,.T.);
#7791=ORIENTED_EDGE('',*,*,#6109,.T.);
#7792=ORIENTED_EDGE('',*,*,#6110,.F.);
#7793=ORIENTED_EDGE('',*,*,#6109,.F.);
#7794=ORIENTED_EDGE('',*,*,#6111,.T.);
#7795=ORIENTED_EDGE('',*,*,#6112,.T.);
#7796=ORIENTED_EDGE('',*,*,#6113,.F.);
#7797=ORIENTED_EDGE('',*,*,#6112,.F.);
#7798=ORIENTED_EDGE('',*,*,#6114,.T.);
#7799=ORIENTED_EDGE('',*,*,#6115,.T.);
#7800=ORIENTED_EDGE('',*,*,#6116,.F.);
#7801=ORIENTED_EDGE('',*,*,#6115,.F.);
#7802=ORIENTED_EDGE('',*,*,#6117,.T.);
#7803=ORIENTED_EDGE('',*,*,#6118,.T.);
#7804=ORIENTED_EDGE('',*,*,#6119,.F.);
#7805=ORIENTED_EDGE('',*,*,#6118,.F.);
#7806=ORIENTED_EDGE('',*,*,#6120,.T.);
#7807=ORIENTED_EDGE('',*,*,#6104,.T.);
#7808=ORIENTED_EDGE('',*,*,#6111,.F.);
#7809=ORIENTED_EDGE('',*,*,#6108,.F.);
#7810=ORIENTED_EDGE('',*,*,#6105,.F.);
#7811=ORIENTED_EDGE('',*,*,#6120,.F.);
#7812=ORIENTED_EDGE('',*,*,#6117,.F.);
#7813=ORIENTED_EDGE('',*,*,#6114,.F.);
#7814=ORIENTED_EDGE('',*,*,#6121,.F.);
#7815=ORIENTED_EDGE('',*,*,#6122,.T.);
#7816=ORIENTED_EDGE('',*,*,#6123,.F.);
#7817=ORIENTED_EDGE('',*,*,#6124,.T.);
#7818=ORIENTED_EDGE('',*,*,#6121,.T.);
#7819=ORIENTED_EDGE('',*,*,#6124,.F.);
#7820=ORIENTED_EDGE('',*,*,#6123,.T.);
#7821=ORIENTED_EDGE('',*,*,#6113,.T.);
#7822=ORIENTED_EDGE('',*,*,#6116,.T.);
#7823=ORIENTED_EDGE('',*,*,#6119,.T.);
#7824=ORIENTED_EDGE('',*,*,#6103,.T.);
#7825=ORIENTED_EDGE('',*,*,#6107,.T.);
#7826=ORIENTED_EDGE('',*,*,#6110,.T.);
#7827=ORIENTED_EDGE('',*,*,#6122,.F.);
#7828=ORIENTED_EDGE('',*,*,#6125,.T.);
#7829=ORIENTED_EDGE('',*,*,#6126,.T.);
#7830=ORIENTED_EDGE('',*,*,#6125,.F.);
#7831=ORIENTED_EDGE('',*,*,#6126,.F.);
#10303=CYLINDRICAL_SURFACE('',#11572,0.275);
#10304=CYLINDRICAL_SURFACE('',#11575,0.15);
#10472=ADVANCED_FACE('',(#1130),#591,.F.);
#10473=ADVANCED_FACE('',(#1131),#592,.F.);
#10474=ADVANCED_FACE('',(#1132),#593,.F.);
#10475=ADVANCED_FACE('',(#1133),#594,.F.);
#10476=ADVANCED_FACE('',(#1134),#595,.F.);
#10477=ADVANCED_FACE('',(#1135),#596,.F.);
#10478=ADVANCED_FACE('',(#1136),#597,.T.);
#10479=ADVANCED_FACE('',(#1137,#450),#598,.F.);
#10480=ADVANCED_FACE('',(#1138),#10303,.T.);
#10481=ADVANCED_FACE('',(#1139,#451),#599,.T.);
#10482=ADVANCED_FACE('',(#1140),#10304,.T.);
#10483=ADVANCED_FACE('',(#1141),#600,.F.);
#10996=CLOSED_SHELL('',(#10472,#10473,#10474,#10475,#10476,#10477,#10478,
#10479,#10480,#10481,#10482,#10483));
#11561=AXIS2_PLACEMENT_3D('',#15914,#12869,#12870);
#11562=AXIS2_PLACEMENT_3D('',#15915,#12871,#12872);
#11563=AXIS2_PLACEMENT_3D('',#15924,#12877,#12878);
#11564=AXIS2_PLACEMENT_3D('',#15930,#12882,#12883);
#11565=AXIS2_PLACEMENT_3D('',#15936,#12887,#12888);
#11566=AXIS2_PLACEMENT_3D('',#15942,#12892,#12893);
#11567=AXIS2_PLACEMENT_3D('',#15948,#12897,#12898);
#11568=AXIS2_PLACEMENT_3D('',#15951,#12901,#12902);
#11569=AXIS2_PLACEMENT_3D('',#15952,#12903,#12904);
#11570=AXIS2_PLACEMENT_3D('',#15954,#12905,#12906);
#11571=AXIS2_PLACEMENT_3D('',#15956,#12907,#12908);
#11572=AXIS2_PLACEMENT_3D('',#15957,#12909,#12910);
#11573=AXIS2_PLACEMENT_3D('',#15959,#12911,#12912);
#11574=AXIS2_PLACEMENT_3D('',#15961,#12914,#12915);
#11575=AXIS2_PLACEMENT_3D('',#15962,#12916,#12917);
#11576=AXIS2_PLACEMENT_3D('',#15965,#12919,#12920);
#11577=AXIS2_PLACEMENT_3D('',#15966,#12921,#12922);
#12869=DIRECTION('axis',(0.,0.,1.));
#12870=DIRECTION('refdir',(1.,0.,0.));
#12871=DIRECTION('center_axis',(-0.866025403784439,0.,0.499999999999999));
#12872=DIRECTION('ref_axis',(0.499999999999999,0.,0.866025403784439));
#12873=DIRECTION('',(-0.499999999999999,0.,-0.866025403784439));
#12874=DIRECTION('',(0.,1.,0.));
#12875=DIRECTION('',(-0.499999999999999,0.,-0.866025403784439));
#12876=DIRECTION('',(0.,1.,0.));
#12877=DIRECTION('center_axis',(-0.86602540378444,0.,-0.499999999999998));
#12878=DIRECTION('ref_axis',(-0.499999999999998,0.,0.86602540378444));
#12879=DIRECTION('',(0.499999999999998,0.,-0.86602540378444));
#12880=DIRECTION('',(0.499999999999998,0.,-0.86602540378444));
#12881=DIRECTION('',(0.,1.,0.));
#12882=DIRECTION('center_axis',(0.,0.,-1.));
#12883=DIRECTION('ref_axis',(-1.,0.,0.));
#12884=DIRECTION('',(1.,0.,0.));
#12885=DIRECTION('',(1.,0.,0.));
#12886=DIRECTION('',(0.,1.,0.));
#12887=DIRECTION('center_axis',(0.866025403784438,0.,-0.5));
#12888=DIRECTION('ref_axis',(-0.5,0.,-0.866025403784438));
#12889=DIRECTION('',(0.5,0.,0.866025403784438));
#12890=DIRECTION('',(0.5,0.,0.866025403784438));
#12891=DIRECTION('',(0.,1.,0.));
#12892=DIRECTION('center_axis',(0.866025403784438,0.,0.5));
#12893=DIRECTION('ref_axis',(0.5,0.,-0.866025403784438));
#12894=DIRECTION('',(-0.5,0.,0.866025403784438));
#12895=DIRECTION('',(-0.5,0.,0.866025403784438));
#12896=DIRECTION('',(0.,1.,0.));
#12897=DIRECTION('center_axis',(0.,0.,1.));
#12898=DIRECTION('ref_axis',(1.,0.,0.));
#12899=DIRECTION('',(-1.,0.,0.));
#12900=DIRECTION('',(-1.,0.,0.));
#12901=DIRECTION('center_axis',(0.,1.,0.));
#12902=DIRECTION('ref_axis',(1.,0.,0.));
#12903=DIRECTION('center_axis',(0.,1.,0.));
#12904=DIRECTION('ref_axis',(1.,0.,0.));
#12905=DIRECTION('center_axis',(0.,1.,0.));
#12906=DIRECTION('ref_axis',(1.,0.,0.));
#12907=DIRECTION('center_axis',(0.,1.,0.));
#12908=DIRECTION('ref_axis',(1.,0.,0.));
#12909=DIRECTION('center_axis',(0.,1.,0.));
#12910=DIRECTION('ref_axis',(1.,0.,0.));
#12911=DIRECTION('center_axis',(0.,1.,0.));
#12912=DIRECTION('ref_axis',(1.,0.,0.));
#12913=DIRECTION('',(0.,-1.,0.));
#12914=DIRECTION('center_axis',(0.,1.,0.));
#12915=DIRECTION('ref_axis',(1.,0.,0.));
#12916=DIRECTION('center_axis',(0.,1.,0.));
#12917=DIRECTION('ref_axis',(1.,0.,0.));
#12918=DIRECTION('',(0.,-1.,0.));
#12919=DIRECTION('center_axis',(0.,1.,0.));
#12920=DIRECTION('ref_axis',(1.,0.,0.));
#12921=DIRECTION('center_axis',(0.,1.,0.));
#12922=DIRECTION('ref_axis',(1.,0.,0.));
#15914=CARTESIAN_POINT('',(0.,0.,0.));
#15915=CARTESIAN_POINT('Origin',(1.40566243270259,-6.9,5.77));
#15916=CARTESIAN_POINT('',(1.4778312163513,-6.7,5.895));
#15917=CARTESIAN_POINT('',(1.40566243270259,-6.7,5.77));
#15918=CARTESIAN_POINT('',(1.42370462861477,-6.7,5.80125));
#15919=CARTESIAN_POINT('',(1.4778312163513,-6.9,5.895));
#15920=CARTESIAN_POINT('',(1.4778312163513,-6.9,5.895));
#15921=CARTESIAN_POINT('',(1.40566243270259,-6.9,5.77));
#15922=CARTESIAN_POINT('',(1.4778312163513,-6.9,5.895));
#15923=CARTESIAN_POINT('',(1.40566243270259,-6.9,5.77));
#15924=CARTESIAN_POINT('Origin',(1.4778312163513,-6.9,5.645));
#15925=CARTESIAN_POINT('',(1.4778312163513,-6.7,5.645));
#15926=CARTESIAN_POINT('',(1.45978902043912,-6.7,5.67625));
#15927=CARTESIAN_POINT('',(1.4778312163513,-6.9,5.645));
#15928=CARTESIAN_POINT('',(1.40566243270259,-6.9,5.77));
#15929=CARTESIAN_POINT('',(1.4778312163513,-6.9,5.645));
#15930=CARTESIAN_POINT('Origin',(1.6221687836487,-6.9,5.645));
#15931=CARTESIAN_POINT('',(1.6221687836487,-6.7,5.645));
#15932=CARTESIAN_POINT('',(1.58608439182435,-6.7,5.645));
#15933=CARTESIAN_POINT('',(1.6221687836487,-6.9,5.645));
#15934=CARTESIAN_POINT('',(1.4778312163513,-6.9,5.645));
#15935=CARTESIAN_POINT('',(1.6221687836487,-6.9,5.645));
#15936=CARTESIAN_POINT('Origin',(1.69433756729741,-6.9,5.77));
#15937=CARTESIAN_POINT('',(1.69433756729741,-6.7,5.77));
#15938=CARTESIAN_POINT('',(1.67629537138523,-6.7,5.73875));
#15939=CARTESIAN_POINT('',(1.69433756729741,-6.9,5.77));
#15940=CARTESIAN_POINT('',(1.6221687836487,-6.9,5.645));
#15941=CARTESIAN_POINT('',(1.69433756729741,-6.9,5.77));
#15942=CARTESIAN_POINT('Origin',(1.6221687836487,-6.9,5.895));
#15943=CARTESIAN_POINT('',(1.6221687836487,-6.7,5.895));
#15944=CARTESIAN_POINT('',(1.64021097956088,-6.7,5.86375));
#15945=CARTESIAN_POINT('',(1.6221687836487,-6.9,5.895));
#15946=CARTESIAN_POINT('',(1.69433756729741,-6.9,5.77));
#15947=CARTESIAN_POINT('',(1.6221687836487,-6.9,5.895));
#15948=CARTESIAN_POINT('Origin',(1.4778312163513,-6.9,5.895));
#15949=CARTESIAN_POINT('',(1.51391560817565,-6.7,5.895));
#15950=CARTESIAN_POINT('',(1.6221687836487,-6.9,5.895));
#15951=CARTESIAN_POINT('Origin',(1.55,-6.9,5.77));
#15952=CARTESIAN_POINT('Origin',(1.55,-7.,5.77));
#15953=CARTESIAN_POINT('',(1.275,-7.,5.77));
#15954=CARTESIAN_POINT('Origin',(1.55,-7.,5.77));
#15955=CARTESIAN_POINT('',(1.4,-7.,5.77));
#15956=CARTESIAN_POINT('Origin',(1.55,-7.,5.77));
#15957=CARTESIAN_POINT('Origin',(1.55,-7.,5.77));
#15958=CARTESIAN_POINT('',(1.275,-6.7,5.77));
#15959=CARTESIAN_POINT('Origin',(1.55,-6.7,5.77));
#15960=CARTESIAN_POINT('',(1.275,-7.,5.77));
#15961=CARTESIAN_POINT('Origin',(1.55,-6.7,5.77));
#15962=CARTESIAN_POINT('Origin',(1.55,-8.,5.77));
#15963=CARTESIAN_POINT('',(1.4,-8.,5.77));
#15964=CARTESIAN_POINT('',(1.4,-8.,5.77));
#15965=CARTESIAN_POINT('Origin',(1.55,-8.,5.77));
#15966=CARTESIAN_POINT('Origin',(1.55,-8.,5.77));
#19300=UNCERTAINTY_MEASURE_WITH_UNIT(LENGTH_MEASURE(0.001),#19362,
'DISTANCE_ACCURACY_VALUE',
'Maximum model space distance between geometric entities at asserted c
onnectivities');
#19323=UNCERTAINTY_MEASURE_WITH_UNIT(LENGTH_MEASURE(0.001),#19362,
'DISTANCE_ACCURACY_VALUE',
'Maximum model space distance between geometric entities at asserted c
onnectivities');
#19338=(
GEOMETRIC_REPRESENTATION_CONTEXT(3)
GLOBAL_UNCERTAINTY_ASSIGNED_CONTEXT((#19300))
GLOBAL_UNIT_ASSIGNED_CONTEXT((#19362,#19364,#19365))
REPRESENTATION_CONTEXT('','3D')
);
#19361=(
GEOMETRIC_REPRESENTATION_CONTEXT(3)
GLOBAL_UNCERTAINTY_ASSIGNED_CONTEXT((#19323))
GLOBAL_UNIT_ASSIGNED_CONTEXT((#19362,#19364,#19365))
REPRESENTATION_CONTEXT('','3D')
);
#19362=(
LENGTH_UNIT()
NAMED_UNIT(*)
SI_UNIT(.CENTI.,.METRE.)
);
#19364=(
NAMED_UNIT(*)
PLANE_ANGLE_UNIT()
SI_UNIT($,.RADIAN.)
);
#19365=(
NAMED_UNIT(*)
SI_UNIT($,.STERADIAN.)
SOLID_ANGLE_UNIT()
);
#19380=SHAPE_DEFINITION_REPRESENTATION(#19417,#19502);
#19417=PRODUCT_DEFINITION_SHAPE('',$,#19540);
#19502=SHAPE_REPRESENTATION('',(#11561),#19338);
#19525=PRODUCT_DEFINITION_CONTEXT('part definition',#19638,'design');
#19540=PRODUCT_DEFINITION('M3x10 motor screw (3)','M3x10 motor screw (3)',
#19577,#19525);
#19577=PRODUCT_DEFINITION_FORMATION('',$,#19654);
#19638=APPLICATION_CONTEXT(
'Core Data for Automotive Mechanical Design Process');
#19639=PRODUCT_CONTEXT('part definition',#19638,'mechanical');
#19654=PRODUCT('M3x10 motor screw (3)','M3x10 motor screw (3)',
'M3x10 motor screw (3)',(#19639));
#19747=COLOUR_RGB('Black',0.12,0.14,0.17);
#19748=FILL_AREA_STYLE_COLOUR('',#19747);
#19749=FILL_AREA_STYLE('',(#19748));
#19750=SURFACE_STYLE_FILL_AREA(#19749);
#19751=SURFACE_SIDE_STYLE('',(#19750));
#19752=SURFACE_STYLE_USAGE(.BOTH.,#19751);
#19753=PRESENTATION_STYLE_ASSIGNMENT((#19752));
ENDSEC;
END-ISO-10303-21;
